ISO-10303-21;
HEADER;
/* Generated by software containing ST-Developer
 * from STEP Tools, Inc. (www.steptools.com) 
 */

FILE_DESCRIPTION(
/* description */ ('Horizontal push-pull toggle clamp'),
/* implementation_level */ '2;1');

FILE_NAME(
/* name */ 'Flat Washer - M6.step',
/* time_stamp */ '2026-10-27T21:21:09-07:00',
/* author */ (''),
/* organization */ (''),
/* preprocessor_version */ 'ST-DEVELOPER v20.2',
/* originating_system */ 'Autodesk Translation Framework v15.17.0.0',
/* authorisation */ '');

FILE_SCHEMA (('AUTOMOTIVE_DESIGN { 1 0 10303 214 3 1 1 }'));
ENDSEC;

DATA;
#10=MECHANICAL_DESIGN_GEOMETRIC_PRESENTATION_REPRESENTATION('',(#195),#4791);
#169=SHAPE_REPRESENTATION_RELATIONSHIP('SRR','None',#4875,#182);
#182=ADVANCED_BREP_SHAPE_REPRESENTATION('',(#207),#4788);
#195=STYLED_ITEM('',(#5030),#207);
#207=MANIFOLD_SOLID_BREP('Body1',#2640);
#251=FACE_BOUND('',#695,.T.);
#252=FACE_BOUND('',#697,.T.);
#355=PLANE('',#3021);
#356=PLANE('',#3022);
#500=FACE_OUTER_BOUND('',#692,.T.);
#501=FACE_OUTER_BOUND('',#693,.T.);
#502=FACE_OUTER_BOUND('',#694,.T.);
#503=FACE_OUTER_BOUND('',#696,.T.);
#692=EDGE_LOOP('',(#2395,#2396,#2397,#2398));
#693=EDGE_LOOP('',(#2399,#2400,#2401,#2402));
#694=EDGE_LOOP('',(#2403));
#695=EDGE_LOOP('',(#2404));
#696=EDGE_LOOP('',(#2405));
#697=EDGE_LOOP('',(#2406));
#783=CIRCLE('',#3016,0.32);
#784=CIRCLE('',#3017,0.32);
#785=CIRCLE('',#3019,0.6);
#786=CIRCLE('',#3020,0.6);
#1007=LINE('',#4626,#1227);
#1008=LINE('',#4632,#1228);
#1227=VECTOR('',#3741,0.32);
#1228=VECTOR('',#3748,0.6);
#1437=VERTEX_POINT('',#4623);
#1438=VERTEX_POINT('',#4625);
#1439=VERTEX_POINT('',#4629);
#1440=VERTEX_POINT('',#4631);
#1759=EDGE_CURVE('',#1437,#1437,#783,.T.);
#1760=EDGE_CURVE('',#1437,#1438,#1007,.T.);
#1761=EDGE_CURVE('',#1438,#1438,#784,.T.);
#1762=EDGE_CURVE('',#1439,#1439,#785,.T.);
#1763=EDGE_CURVE('',#1439,#1440,#1008,.T.);
#1764=EDGE_CURVE('',#1440,#1440,#786,.T.);
#2395=ORIENTED_EDGE('',*,*,#1759,.F.);
#2396=ORIENTED_EDGE('',*,*,#1760,.T.);
#2397=ORIENTED_EDGE('',*,*,#1761,.T.);
#2398=ORIENTED_EDGE('',*,*,#1760,.F.);
#2399=ORIENTED_EDGE('',*,*,#1762,.F.);
#2400=ORIENTED_EDGE('',*,*,#1763,.T.);
#2401=ORIENTED_EDGE('',*,*,#1764,.T.);
#2402=ORIENTED_EDGE('',*,*,#1763,.F.);
#2403=ORIENTED_EDGE('',*,*,#1762,.T.);
#2404=ORIENTED_EDGE('',*,*,#1759,.T.);
#2405=ORIENTED_EDGE('',*,*,#1764,.F.);
#2406=ORIENTED_EDGE('',*,*,#1761,.F.);
#2473=CYLINDRICAL_SURFACE('',#3015,0.32);
#2474=CYLINDRICAL_SURFACE('',#3018,0.6);
#2616=ADVANCED_FACE('',(#500),#2473,.F.);
#2617=ADVANCED_FACE('',(#501),#2474,.T.);
#2618=ADVANCED_FACE('',(#502,#251),#355,.T.);
#2619=ADVANCED_FACE('',(#503,#252),#356,.F.);
#2640=CLOSED_SHELL('',(#2616,#2617,#2618,#2619));
#3014=AXIS2_PLACEMENT_3D('',#4621,#3735,#3736);
#3015=AXIS2_PLACEMENT_3D('',#4622,#3737,#3738);
#3016=AXIS2_PLACEMENT_3D('',#4624,#3739,#3740);
#3017=AXIS2_PLACEMENT_3D('',#4627,#3742,#3743);
#3018=AXIS2_PLACEMENT_3D('',#4628,#3744,#3745);
#3019=AXIS2_PLACEMENT_3D('',#4630,#3746,#3747);
#3020=AXIS2_PLACEMENT_3D('',#4633,#3749,#3750);
#3021=AXIS2_PLACEMENT_3D('',#4634,#3751,#3752);
#3022=AXIS2_PLACEMENT_3D('',#4635,#3753,#3754);
#3735=DIRECTION('axis',(0.,0.,1.));
#3736=DIRECTION('refdir',(1.,0.,0.));
#3737=DIRECTION('center_axis',(0.,1.,0.));
#3738=DIRECTION('ref_axis',(1.,0.,0.));
#3739=DIRECTION('center_axis',(0.,-1.,0.));
#3740=DIRECTION('ref_axis',(1.,0.,0.));
#3741=DIRECTION('',(0.,-1.,0.));
#3742=DIRECTION('center_axis',(0.,-1.,0.));
#3743=DIRECTION('ref_axis',(1.,0.,0.));
#3744=DIRECTION('center_axis',(0.,1.,0.));
#3745=DIRECTION('ref_axis',(1.,0.,0.));
#3746=DIRECTION('center_axis',(0.,1.,0.));
#3747=DIRECTION('ref_axis',(1.,0.,0.));
#3748=DIRECTION('',(0.,-1.,0.));
#3749=DIRECTION('center_axis',(0.,1.,0.));
#3750=DIRECTION('ref_axis',(1.,0.,0.));
#3751=DIRECTION('center_axis',(0.,1.,0.));
#3752=DIRECTION('ref_axis',(1.,0.,0.));
#3753=DIRECTION('center_axis',(0.,1.,0.));
#3754=DIRECTION('ref_axis',(1.,0.,0.));
#4621=CARTESIAN_POINT('',(0.,0.,0.));
#4622=CARTESIAN_POINT('Origin',(0.,0.,0.));
#4623=CARTESIAN_POINT('',(-0.32,0.16,3.91886975727153E-17));
#4624=CARTESIAN_POINT('Origin',(0.,0.16,0.));
#4625=CARTESIAN_POINT('',(-0.32,0.,3.91886975727153E-17));
#4626=CARTESIAN_POINT('',(-0.32,0.,3.91886975727153E-17));
#4627=CARTESIAN_POINT('Origin',(0.,0.,0.));
#4628=CARTESIAN_POINT('Origin',(0.,0.,0.));
#4629=CARTESIAN_POINT('',(-0.6,0.16,7.34788079488412E-17));
#4630=CARTESIAN_POINT('Origin',(0.,0.16,0.));
#4631=CARTESIAN_POINT('',(-0.6,0.,7.34788079488412E-17));
#4632=CARTESIAN_POINT('',(-0.6,0.,7.34788079488412E-17));
#4633=CARTESIAN_POINT('Origin',(0.,0.,0.));
#4634=CARTESIAN_POINT('Origin',(0.,0.16,0.));
#4635=CARTESIAN_POINT('Origin',(0.,0.,0.));
#4769=UNCERTAINTY_MEASURE_WITH_UNIT(LENGTH_MEASURE(0.001),#4792,
'DISTANCE_ACCURACY_VALUE',
'Maximum model space distance between geometric entities at asserted c
onnectivities');
#4772=UNCERTAINTY_MEASURE_WITH_UNIT(LENGTH_MEASURE(0.001),#4792,
'DISTANCE_ACCURACY_VALUE',
'Maximum model space distance between geometric entities at asserted c
onnectivities');
#4788=(
GEOMETRIC_REPRESENTATION_CONTEXT(3)
GLOBAL_UNCERTAINTY_ASSIGNED_CONTEXT((#4769))
GLOBAL_UNIT_ASSIGNED_CONTEXT((#4792,#4794,#4795))
REPRESENTATION_CONTEXT('','3D')
);
#4791=(
GEOMETRIC_REPRESENTATION_CONTEXT(3)
GLOBAL_UNCERTAINTY_ASSIGNED_CONTEXT((#4772))
GLOBAL_UNIT_ASSIGNED_CONTEXT((#4792,#4794,#4795))
REPRESENTATION_CONTEXT('','3D')
);
#4792=(
LENGTH_UNIT()
NAMED_UNIT(*)
SI_UNIT(.CENTI.,.METRE.)
);
#4794=(
NAMED_UNIT(*)
PLANE_ANGLE_UNIT()
SI_UNIT($,.RADIAN.)
);
#4795=(
NAMED_UNIT(*)
SI_UNIT($,.STERADIAN.)
SOLID_ANGLE_UNIT()
);
#4811=SHAPE_DEFINITION_REPRESENTATION(#4830,#4875);
#4830=PRODUCT_DEFINITION_SHAPE('',$,#4894);
#4875=SHAPE_REPRESENTATION('',(#3014),#4788);
#4878=PRODUCT_DEFINITION_CONTEXT('part definition',#4934,'design');
#4894=PRODUCT_DEFINITION('Flat Washer - M6','Flat Washer - M6',#4912,#4878);
#4912=PRODUCT_DEFINITION_FORMATION('',$,#4951);
#4934=APPLICATION_CONTEXT(
'Core Data for Automotive Mechanical Design Process');
#4935=PRODUCT_CONTEXT('part definition',#4934,'mechanical');
#4951=PRODUCT('Flat Washer - M6','Flat Washer - M6','Flat Washer - M6',
(#4935));
#5024=COLOUR_RGB('Black',0.12,0.14,0.17);
#5025=FILL_AREA_STYLE_COLOUR('',#5024);
#5026=FILL_AREA_STYLE('',(#5025));
#5027=SURFACE_STYLE_FILL_AREA(#5026);
#5028=SURFACE_SIDE_STYLE('',(#5027));
#5029=SURFACE_STYLE_USAGE(.BOTH.,#5028);
#5030=PRESENTATION_STYLE_ASSIGNMENT((#5029));
ENDSEC;
END-ISO-10303-21;
